ISO-10303-21;
HEADER;
/* Generated by software containing ST-Developer
 * from STEP Tools, Inc. (www.steptools.com) 
 */

FILE_DESCRIPTION(
/* description */ ('STEP AP214'),
/* implementation_level */ '2;1');

FILE_NAME(
/* name */ 'Washer.step',
/* time_stamp */ '2026-11-15T14:49:54-08:00',
/* author */ (''),
/* organization */ (''),
/* preprocessor_version */ 'ST-DEVELOPER v20.2',
/* originating_system */ 'Autodesk Translation Framework v15.17.0.0',
/* authorisation */ '');

FILE_SCHEMA (('AUTOMOTIVE_DESIGN { 1 0 10303 214 3 1 1 }'));
ENDSEC;

DATA;
#10=MECHANICAL_DESIGN_GEOMETRIC_PRESENTATION_REPRESENTATION('',(#1110),#66721);
#1048=SHAPE_REPRESENTATION_RELATIONSHIP('SRR','None',#66908,#1079);
#1079=ADVANCED_BREP_SHAPE_REPRESENTATION('',(#1145),#66699);
#1110=STYLED_ITEM('',(#67095),#1145);
#1145=MANIFOLD_SOLID_BREP('Body1',#25676);
#1338=FACE_BOUND('',#4577,.T.);
#1339=FACE_BOUND('',#4578,.T.);
#1340=FACE_BOUND('',#4580,.T.);
#1341=FACE_BOUND('',#4581,.T.);
#1907=PLANE('',#27448);
#1908=PLANE('',#27453);
#1909=PLANE('',#27458);
#1910=PLANE('',#27460);
#1911=PLANE('',#27463);
#1912=PLANE('',#27465);
#1913=PLANE('',#27466);
#1914=PLANE('',#27467);
#2960=FACE_OUTER_BOUND('',#4572,.T.);
#2961=FACE_OUTER_BOUND('',#4573,.T.);
#2962=FACE_OUTER_BOUND('',#4574,.T.);
#2963=FACE_OUTER_BOUND('',#4575,.T.);
#2964=FACE_OUTER_BOUND('',#4576,.T.);
#2965=FACE_OUTER_BOUND('',#4579,.T.);
#2966=FACE_OUTER_BOUND('',#4582,.T.);
#2967=FACE_OUTER_BOUND('',#4583,.T.);
#2968=FACE_OUTER_BOUND('',#4584,.T.);
#2969=FACE_OUTER_BOUND('',#4585,.T.);
#2970=FACE_OUTER_BOUND('',#4586,.T.);
#2971=FACE_OUTER_BOUND('',#4587,.T.);
#2972=FACE_OUTER_BOUND('',#4588,.T.);
#2973=FACE_OUTER_BOUND('',#4589,.T.);
#2974=FACE_OUTER_BOUND('',#4590,.T.);
#2975=FACE_OUTER_BOUND('',#4591,.T.);
#4572=EDGE_LOOP('',(#20330,#20331,#20332,#20333));
#4573=EDGE_LOOP('',(#20334,#20335,#20336,#20337));
#4574=EDGE_LOOP('',(#20338,#20339,#20340,#20341));
#4575=EDGE_LOOP('',(#20342,#20343,#20344,#20345));
#4576=EDGE_LOOP('',(#20346,#20347,#20348,#20349,#20350,#20351,#20352,#20353,
#20354,#20355,#20356,#20357));
#4577=EDGE_LOOP('',(#20358));
#4578=EDGE_LOOP('',(#20359));
#4579=EDGE_LOOP('',(#20360,#20361,#20362,#20363,#20364,#20365,#20366,#20367,
#20368,#20369,#20370,#20371));
#4580=EDGE_LOOP('',(#20372));
#4581=EDGE_LOOP('',(#20373));
#4582=EDGE_LOOP('',(#20374,#20375,#20376,#20377));
#4583=EDGE_LOOP('',(#20378,#20379,#20380,#20381));
#4584=EDGE_LOOP('',(#20382,#20383,#20384,#20385));
#4585=EDGE_LOOP('',(#20386,#20387,#20388,#20389));
#4586=EDGE_LOOP('',(#20390,#20391,#20392,#20393));
#4587=EDGE_LOOP('',(#20394,#20395,#20396,#20397));
#4588=EDGE_LOOP('',(#20398,#20399,#20400,#20401));
#4589=EDGE_LOOP('',(#20402,#20403,#20404,#20405));
#4590=EDGE_LOOP('',(#20406,#20407,#20408,#20409));
#4591=EDGE_LOOP('',(#20410,#20411,#20412,#20413));
#6632=LINE('',#40339,#8621);
#6633=LINE('',#40345,#8622);
#6634=LINE('',#40352,#8623);
#6635=LINE('',#40355,#8624);
#6636=LINE('',#40361,#8625);
#6637=LINE('',#40364,#8626);
#6638=LINE('',#40368,#8627);
#6639=LINE('',#40372,#8628);
#6640=LINE('',#40377,#8629);
#6641=LINE('',#40381,#8630);
#6642=LINE('',#40382,#8631);
#6643=LINE('',#40383,#8632);
#6644=LINE('',#40387,#8633);
#6645=LINE('',#40388,#8634);
#6646=LINE('',#40390,#8635);
#6647=LINE('',#40392,#8636);
#6648=LINE('',#40396,#8637);
#6649=LINE('',#40401,#8638);
#6650=LINE('',#40404,#8639);
#6651=LINE('',#40405,#8640);
#6652=LINE('',#40407,#8641);
#6653=LINE('',#40409,#8642);
#6654=LINE('',#40412,#8643);
#6655=LINE('',#40414,#8644);
#6656=LINE('',#40416,#8645);
#6657=LINE('',#40418,#8646);
#8621=VECTOR('',#32699,0.85);
#8622=VECTOR('',#32706,0.85);
#8623=VECTOR('',#32713,1000.);
#8624=VECTOR('',#32716,1000.);
#8625=VECTOR('',#32721,1000.);
#8626=VECTOR('',#32724,1000.);
#8627=VECTOR('',#32727,1000.);
#8628=VECTOR('',#32730,1000.);
#8629=VECTOR('',#32735,1000.);
#8630=VECTOR('',#32738,1000.);
#8631=VECTOR('',#32739,1000.);
#8632=VECTOR('',#32740,1000.);
#8633=VECTOR('',#32743,1000.);
#8634=VECTOR('',#32744,1000.);
#8635=VECTOR('',#32745,1000.);
#8636=VECTOR('',#32746,1000.);
#8637=VECTOR('',#32749,1000.);
#8638=VECTOR('',#32754,1000.);
#8639=VECTOR('',#32759,1000.);
#8640=VECTOR('',#32760,1000.);
#8641=VECTOR('',#32763,1000.);
#8642=VECTOR('',#32766,1000.);
#8643=VECTOR('',#32771,1000.);
#8644=VECTOR('',#32774,1000.);
#8645=VECTOR('',#32777,1000.);
#8646=VECTOR('',#32780,1000.);
#10058=CIRCLE('',#27437,0.85);
#10059=CIRCLE('',#27438,0.85);
#10060=CIRCLE('',#27440,0.85);
#10061=CIRCLE('',#27441,0.85);
#10062=CIRCLE('',#27443,7.15);
#10063=CIRCLE('',#27444,7.15);
#10064=CIRCLE('',#27446,8.8);
#10065=CIRCLE('',#27447,8.8);
#10066=CIRCLE('',#27449,1.9);
#10067=CIRCLE('',#27450,1.9);
#10068=CIRCLE('',#27451,1.9);
#10069=CIRCLE('',#27452,1.9);
#10070=CIRCLE('',#27454,1.9);
#10071=CIRCLE('',#27455,1.9);
#10072=CIRCLE('',#27456,1.9);
#10073=CIRCLE('',#27457,1.9);
#11873=VERTEX_POINT('',#40336);
#11874=VERTEX_POINT('',#40338);
#11875=VERTEX_POINT('',#40342);
#11876=VERTEX_POINT('',#40344);
#11877=VERTEX_POINT('',#40348);
#11878=VERTEX_POINT('',#40349);
#11879=VERTEX_POINT('',#40351);
#11880=VERTEX_POINT('',#40353);
#11881=VERTEX_POINT('',#40357);
#11882=VERTEX_POINT('',#40358);
#11883=VERTEX_POINT('',#40360);
#11884=VERTEX_POINT('',#40362);
#11885=VERTEX_POINT('',#40366);
#11886=VERTEX_POINT('',#40367);
#11887=VERTEX_POINT('',#40369);
#11888=VERTEX_POINT('',#40371);
#11889=VERTEX_POINT('',#40374);
#11890=VERTEX_POINT('',#40376);
#11891=VERTEX_POINT('',#40378);
#11892=VERTEX_POINT('',#40380);
#11893=VERTEX_POINT('',#40385);
#11894=VERTEX_POINT('',#40386);
#11895=VERTEX_POINT('',#40389);
#11896=VERTEX_POINT('',#40391);
#11897=VERTEX_POINT('',#40393);
#11898=VERTEX_POINT('',#40395);
#11899=VERTEX_POINT('',#40398);
#11900=VERTEX_POINT('',#40400);
#14858=EDGE_CURVE('',#11873,#11873,#10058,.T.);
#14859=EDGE_CURVE('',#11873,#11874,#6632,.T.);
#14860=EDGE_CURVE('',#11874,#11874,#10059,.T.);
#14861=EDGE_CURVE('',#11875,#11875,#10060,.T.);
#14862=EDGE_CURVE('',#11875,#11876,#6633,.T.);
#14863=EDGE_CURVE('',#11876,#11876,#10061,.T.);
#14864=EDGE_CURVE('',#11877,#11878,#10062,.T.);
#14865=EDGE_CURVE('',#11877,#11879,#6634,.T.);
#14866=EDGE_CURVE('',#11879,#11880,#10063,.T.);
#14867=EDGE_CURVE('',#11878,#11880,#6635,.T.);
#14868=EDGE_CURVE('',#11881,#11882,#10064,.T.);
#14869=EDGE_CURVE('',#11881,#11883,#6636,.T.);
#14870=EDGE_CURVE('',#11883,#11884,#10065,.T.);
#14871=EDGE_CURVE('',#11882,#11884,#6637,.T.);
#14872=EDGE_CURVE('',#11885,#11886,#6638,.T.);
#14873=EDGE_CURVE('',#11886,#11887,#10066,.T.);
#14874=EDGE_CURVE('',#11887,#11888,#6639,.T.);
#14875=EDGE_CURVE('',#11888,#11881,#10067,.T.);
#14876=EDGE_CURVE('',#11882,#11889,#10068,.T.);
#14877=EDGE_CURVE('',#11889,#11890,#6640,.T.);
#14878=EDGE_CURVE('',#11890,#11891,#10069,.T.);
#14879=EDGE_CURVE('',#11891,#11892,#6641,.T.);
#14880=EDGE_CURVE('',#11892,#11877,#6642,.T.);
#14881=EDGE_CURVE('',#11878,#11885,#6643,.T.);
#14882=EDGE_CURVE('',#11893,#11894,#6644,.T.);
#14883=EDGE_CURVE('',#11880,#11893,#6645,.T.);
#14884=EDGE_CURVE('',#11895,#11879,#6646,.T.);
#14885=EDGE_CURVE('',#11896,#11895,#6647,.T.);
#14886=EDGE_CURVE('',#11897,#11896,#10070,.T.);
#14887=EDGE_CURVE('',#11898,#11897,#6648,.T.);
#14888=EDGE_CURVE('',#11884,#11898,#10071,.T.);
#14889=EDGE_CURVE('',#11899,#11883,#10072,.T.);
#14890=EDGE_CURVE('',#11900,#11899,#6649,.T.);
#14891=EDGE_CURVE('',#11894,#11900,#10073,.T.);
#14892=EDGE_CURVE('',#11886,#11894,#6650,.T.);
#14893=EDGE_CURVE('',#11885,#11893,#6651,.T.);
#14894=EDGE_CURVE('',#11887,#11900,#6652,.T.);
#14895=EDGE_CURVE('',#11888,#11899,#6653,.T.);
#14896=EDGE_CURVE('',#11889,#11898,#6654,.T.);
#14897=EDGE_CURVE('',#11890,#11897,#6655,.T.);
#14898=EDGE_CURVE('',#11891,#11896,#6656,.T.);
#14899=EDGE_CURVE('',#11892,#11895,#6657,.T.);
#20330=ORIENTED_EDGE('',*,*,#14858,.T.);
#20331=ORIENTED_EDGE('',*,*,#14859,.T.);
#20332=ORIENTED_EDGE('',*,*,#14860,.F.);
#20333=ORIENTED_EDGE('',*,*,#14859,.F.);
#20334=ORIENTED_EDGE('',*,*,#14861,.T.);
#20335=ORIENTED_EDGE('',*,*,#14862,.T.);
#20336=ORIENTED_EDGE('',*,*,#14863,.F.);
#20337=ORIENTED_EDGE('',*,*,#14862,.F.);
#20338=ORIENTED_EDGE('',*,*,#14864,.F.);
#20339=ORIENTED_EDGE('',*,*,#14865,.T.);
#20340=ORIENTED_EDGE('',*,*,#14866,.T.);
#20341=ORIENTED_EDGE('',*,*,#14867,.F.);
#20342=ORIENTED_EDGE('',*,*,#14868,.F.);
#20343=ORIENTED_EDGE('',*,*,#14869,.T.);
#20344=ORIENTED_EDGE('',*,*,#14870,.T.);
#20345=ORIENTED_EDGE('',*,*,#14871,.F.);
#20346=ORIENTED_EDGE('',*,*,#14872,.T.);
#20347=ORIENTED_EDGE('',*,*,#14873,.T.);
#20348=ORIENTED_EDGE('',*,*,#14874,.T.);
#20349=ORIENTED_EDGE('',*,*,#14875,.T.);
#20350=ORIENTED_EDGE('',*,*,#14868,.T.);
#20351=ORIENTED_EDGE('',*,*,#14876,.T.);
#20352=ORIENTED_EDGE('',*,*,#14877,.T.);
#20353=ORIENTED_EDGE('',*,*,#14878,.T.);
#20354=ORIENTED_EDGE('',*,*,#14879,.T.);
#20355=ORIENTED_EDGE('',*,*,#14880,.T.);
#20356=ORIENTED_EDGE('',*,*,#14864,.T.);
#20357=ORIENTED_EDGE('',*,*,#14881,.T.);
#20358=ORIENTED_EDGE('',*,*,#14858,.F.);
#20359=ORIENTED_EDGE('',*,*,#14861,.F.);
#20360=ORIENTED_EDGE('',*,*,#14882,.F.);
#20361=ORIENTED_EDGE('',*,*,#14883,.F.);
#20362=ORIENTED_EDGE('',*,*,#14866,.F.);
#20363=ORIENTED_EDGE('',*,*,#14884,.F.);
#20364=ORIENTED_EDGE('',*,*,#14885,.F.);
#20365=ORIENTED_EDGE('',*,*,#14886,.F.);
#20366=ORIENTED_EDGE('',*,*,#14887,.F.);
#20367=ORIENTED_EDGE('',*,*,#14888,.F.);
#20368=ORIENTED_EDGE('',*,*,#14870,.F.);
#20369=ORIENTED_EDGE('',*,*,#14889,.F.);
#20370=ORIENTED_EDGE('',*,*,#14890,.F.);
#20371=ORIENTED_EDGE('',*,*,#14891,.F.);
#20372=ORIENTED_EDGE('',*,*,#14863,.T.);
#20373=ORIENTED_EDGE('',*,*,#14860,.T.);
#20374=ORIENTED_EDGE('',*,*,#14882,.T.);
#20375=ORIENTED_EDGE('',*,*,#14892,.F.);
#20376=ORIENTED_EDGE('',*,*,#14872,.F.);
#20377=ORIENTED_EDGE('',*,*,#14893,.T.);
#20378=ORIENTED_EDGE('',*,*,#14891,.T.);
#20379=ORIENTED_EDGE('',*,*,#14894,.F.);
#20380=ORIENTED_EDGE('',*,*,#14873,.F.);
#20381=ORIENTED_EDGE('',*,*,#14892,.T.);
#20382=ORIENTED_EDGE('',*,*,#14890,.T.);
#20383=ORIENTED_EDGE('',*,*,#14895,.F.);
#20384=ORIENTED_EDGE('',*,*,#14874,.F.);
#20385=ORIENTED_EDGE('',*,*,#14894,.T.);
#20386=ORIENTED_EDGE('',*,*,#14889,.T.);
#20387=ORIENTED_EDGE('',*,*,#14869,.F.);
#20388=ORIENTED_EDGE('',*,*,#14875,.F.);
#20389=ORIENTED_EDGE('',*,*,#14895,.T.);
#20390=ORIENTED_EDGE('',*,*,#14888,.T.);
#20391=ORIENTED_EDGE('',*,*,#14896,.F.);
#20392=ORIENTED_EDGE('',*,*,#14876,.F.);
#20393=ORIENTED_EDGE('',*,*,#14871,.T.);
#20394=ORIENTED_EDGE('',*,*,#14887,.T.);
#20395=ORIENTED_EDGE('',*,*,#14897,.F.);
#20396=ORIENTED_EDGE('',*,*,#14877,.F.);
#20397=ORIENTED_EDGE('',*,*,#14896,.T.);
#20398=ORIENTED_EDGE('',*,*,#14886,.T.);
#20399=ORIENTED_EDGE('',*,*,#14898,.F.);
#20400=ORIENTED_EDGE('',*,*,#14878,.F.);
#20401=ORIENTED_EDGE('',*,*,#14897,.T.);
#20402=ORIENTED_EDGE('',*,*,#14885,.T.);
#20403=ORIENTED_EDGE('',*,*,#14899,.F.);
#20404=ORIENTED_EDGE('',*,*,#14879,.F.);
#20405=ORIENTED_EDGE('',*,*,#14898,.T.);
#20406=ORIENTED_EDGE('',*,*,#14884,.T.);
#20407=ORIENTED_EDGE('',*,*,#14865,.F.);
#20408=ORIENTED_EDGE('',*,*,#14880,.F.);
#20409=ORIENTED_EDGE('',*,*,#14899,.T.);
#20410=ORIENTED_EDGE('',*,*,#14883,.T.);
#20411=ORIENTED_EDGE('',*,*,#14893,.F.);
#20412=ORIENTED_EDGE('',*,*,#14881,.F.);
#20413=ORIENTED_EDGE('',*,*,#14867,.T.);
#24049=CYLINDRICAL_SURFACE('',#27436,0.85);
#24050=CYLINDRICAL_SURFACE('',#27439,0.85);
#24051=CYLINDRICAL_SURFACE('',#27442,7.15);
#24052=CYLINDRICAL_SURFACE('',#27445,8.8);
#24053=CYLINDRICAL_SURFACE('',#27459,1.9);
#24054=CYLINDRICAL_SURFACE('',#27461,1.9);
#24055=CYLINDRICAL_SURFACE('',#27462,1.9);
#24056=CYLINDRICAL_SURFACE('',#27464,1.9);
#24913=ADVANCED_FACE('',(#2960),#24049,.F.);
#24914=ADVANCED_FACE('',(#2961),#24050,.F.);
#24915=ADVANCED_FACE('',(#2962),#24051,.F.);
#24916=ADVANCED_FACE('',(#2963),#24052,.T.);
#24917=ADVANCED_FACE('',(#2964,#1338,#1339),#1907,.T.);
#24918=ADVANCED_FACE('',(#2965,#1340,#1341),#1908,.F.);
#24919=ADVANCED_FACE('',(#2966),#1909,.F.);
#24920=ADVANCED_FACE('',(#2967),#24053,.T.);
#24921=ADVANCED_FACE('',(#2968),#1910,.F.);
#24922=ADVANCED_FACE('',(#2969),#24054,.F.);
#24923=ADVANCED_FACE('',(#2970),#24055,.F.);
#24924=ADVANCED_FACE('',(#2971),#1911,.F.);
#24925=ADVANCED_FACE('',(#2972),#24056,.T.);
#24926=ADVANCED_FACE('',(#2973),#1912,.F.);
#24927=ADVANCED_FACE('',(#2974),#1913,.F.);
#24928=ADVANCED_FACE('',(#2975),#1914,.F.);
#25676=CLOSED_SHELL('',(#24913,#24914,#24915,#24916,#24917,#24918,#24919,
#24920,#24921,#24922,#24923,#24924,#24925,#24926,#24927,#24928));
#27435=AXIS2_PLACEMENT_3D('',#40334,#32693,#32694);
#27436=AXIS2_PLACEMENT_3D('',#40335,#32695,#32696);
#27437=AXIS2_PLACEMENT_3D('',#40337,#32697,#32698);
#27438=AXIS2_PLACEMENT_3D('',#40340,#32700,#32701);
#27439=AXIS2_PLACEMENT_3D('',#40341,#32702,#32703);
#27440=AXIS2_PLACEMENT_3D('',#40343,#32704,#32705);
#27441=AXIS2_PLACEMENT_3D('',#40346,#32707,#32708);
#27442=AXIS2_PLACEMENT_3D('',#40347,#32709,#32710);
#27443=AXIS2_PLACEMENT_3D('',#40350,#32711,#32712);
#27444=AXIS2_PLACEMENT_3D('',#40354,#32714,#32715);
#27445=AXIS2_PLACEMENT_3D('',#40356,#32717,#32718);
#27446=AXIS2_PLACEMENT_3D('',#40359,#32719,#32720);
#27447=AXIS2_PLACEMENT_3D('',#40363,#32722,#32723);
#27448=AXIS2_PLACEMENT_3D('',#40365,#32725,#32726);
#27449=AXIS2_PLACEMENT_3D('',#40370,#32728,#32729);
#27450=AXIS2_PLACEMENT_3D('',#40373,#32731,#32732);
#27451=AXIS2_PLACEMENT_3D('',#40375,#32733,#32734);
#27452=AXIS2_PLACEMENT_3D('',#40379,#32736,#32737);
#27453=AXIS2_PLACEMENT_3D('',#40384,#32741,#32742);
#27454=AXIS2_PLACEMENT_3D('',#40394,#32747,#32748);
#27455=AXIS2_PLACEMENT_3D('',#40397,#32750,#32751);
#27456=AXIS2_PLACEMENT_3D('',#40399,#32752,#32753);
#27457=AXIS2_PLACEMENT_3D('',#40402,#32755,#32756);
#27458=AXIS2_PLACEMENT_3D('',#40403,#32757,#32758);
#27459=AXIS2_PLACEMENT_3D('',#40406,#32761,#32762);
#27460=AXIS2_PLACEMENT_3D('',#40408,#32764,#32765);
#27461=AXIS2_PLACEMENT_3D('',#40410,#32767,#32768);
#27462=AXIS2_PLACEMENT_3D('',#40411,#32769,#32770);
#27463=AXIS2_PLACEMENT_3D('',#40413,#32772,#32773);
#27464=AXIS2_PLACEMENT_3D('',#40415,#32775,#32776);
#27465=AXIS2_PLACEMENT_3D('',#40417,#32778,#32779);
#27466=AXIS2_PLACEMENT_3D('',#40419,#32781,#32782);
#27467=AXIS2_PLACEMENT_3D('',#40420,#32783,#32784);
#32693=DIRECTION('axis',(0.,0.,1.));
#32694=DIRECTION('refdir',(1.,0.,0.));
#32695=DIRECTION('center_axis',(-1.,0.,0.));
#32696=DIRECTION('ref_axis',(0.,0.,1.));
#32697=DIRECTION('center_axis',(1.,0.,0.));
#32698=DIRECTION('ref_axis',(0.,0.,-1.));
#32699=DIRECTION('',(-1.,0.,0.));
#32700=DIRECTION('center_axis',(1.,0.,0.));
#32701=DIRECTION('ref_axis',(0.,0.,-1.));
#32702=DIRECTION('center_axis',(-1.,0.,0.));
#32703=DIRECTION('ref_axis',(0.,0.,1.));
#32704=DIRECTION('center_axis',(1.,0.,0.));
#32705=DIRECTION('ref_axis',(0.,0.,-1.));
#32706=DIRECTION('',(-1.,0.,0.));
#32707=DIRECTION('center_axis',(1.,0.,0.));
#32708=DIRECTION('ref_axis',(0.,0.,-1.));
#32709=DIRECTION('center_axis',(-1.,0.,0.));
#32710=DIRECTION('ref_axis',(0.,1.,6.12323399573677E-17));
#32711=DIRECTION('center_axis',(-1.,0.,0.));
#32712=DIRECTION('ref_axis',(0.,0.,-1.));
#32713=DIRECTION('',(-1.,0.,0.));
#32714=DIRECTION('center_axis',(-1.,0.,0.));
#32715=DIRECTION('ref_axis',(0.,0.,-1.));
#32716=DIRECTION('',(-1.,0.,0.));
#32717=DIRECTION('center_axis',(-1.,0.,0.));
#32718=DIRECTION('ref_axis',(0.,1.,6.12323399573676E-17));
#32719=DIRECTION('center_axis',(1.,0.,0.));
#32720=DIRECTION('ref_axis',(0.,0.,-1.));
#32721=DIRECTION('',(-1.,0.,0.));
#32722=DIRECTION('center_axis',(1.,0.,0.));
#32723=DIRECTION('ref_axis',(0.,0.,-1.));
#32724=DIRECTION('',(-1.,0.,0.));
#32725=DIRECTION('center_axis',(1.,0.,0.));
#32726=DIRECTION('ref_axis',(0.,0.,-1.));
#32727=DIRECTION('',(0.,0.,-1.));
#32728=DIRECTION('center_axis',(1.,0.,0.));
#32729=DIRECTION('ref_axis',(0.,0.,-1.));
#32730=DIRECTION('',(0.,1.,0.));
#32731=DIRECTION('center_axis',(-1.,0.,0.));
#32732=DIRECTION('ref_axis',(0.,0.,-1.));
#32733=DIRECTION('center_axis',(-1.,0.,0.));
#32734=DIRECTION('ref_axis',(0.,0.,-1.));
#32735=DIRECTION('',(0.,-1.,0.));
#32736=DIRECTION('center_axis',(1.,0.,0.));
#32737=DIRECTION('ref_axis',(0.,0.,-1.));
#32738=DIRECTION('',(0.,0.,-1.));
#32739=DIRECTION('',(0.,1.,-1.23292219708887E-16));
#32740=DIRECTION('',(0.,-1.,-1.23292219708887E-16));
#32741=DIRECTION('center_axis',(1.,0.,0.));
#32742=DIRECTION('ref_axis',(0.,0.,-1.));
#32743=DIRECTION('',(0.,0.,-1.));
#32744=DIRECTION('',(0.,-1.,-1.23292219708887E-16));
#32745=DIRECTION('',(0.,1.,-1.23292219708887E-16));
#32746=DIRECTION('',(0.,0.,-1.));
#32747=DIRECTION('center_axis',(1.,0.,0.));
#32748=DIRECTION('ref_axis',(0.,0.,-1.));
#32749=DIRECTION('',(0.,-1.,0.));
#32750=DIRECTION('center_axis',(-1.,0.,0.));
#32751=DIRECTION('ref_axis',(0.,0.,-1.));
#32752=DIRECTION('center_axis',(-1.,0.,0.));
#32753=DIRECTION('ref_axis',(0.,0.,-1.));
#32754=DIRECTION('',(0.,1.,0.));
#32755=DIRECTION('center_axis',(1.,0.,0.));
#32756=DIRECTION('ref_axis',(0.,0.,-1.));
#32757=DIRECTION('center_axis',(0.,1.,0.));
#32758=DIRECTION('ref_axis',(0.,0.,1.));
#32759=DIRECTION('',(-1.,0.,0.));
#32760=DIRECTION('',(-1.,0.,0.));
#32761=DIRECTION('center_axis',(-1.,0.,0.));
#32762=DIRECTION('ref_axis',(0.,0.,1.));
#32763=DIRECTION('',(-1.,0.,0.));
#32764=DIRECTION('center_axis',(0.,0.,1.));
#32765=DIRECTION('ref_axis',(1.,0.,0.));
#32766=DIRECTION('',(-1.,0.,0.));
#32767=DIRECTION('center_axis',(-1.,0.,0.));
#32768=DIRECTION('ref_axis',(0.,0.,1.));
#32769=DIRECTION('center_axis',(-1.,0.,0.));
#32770=DIRECTION('ref_axis',(0.,0.,1.));
#32771=DIRECTION('',(-1.,0.,0.));
#32772=DIRECTION('center_axis',(0.,0.,-1.));
#32773=DIRECTION('ref_axis',(-1.,0.,0.));
#32774=DIRECTION('',(-1.,0.,0.));
#32775=DIRECTION('center_axis',(-1.,0.,0.));
#32776=DIRECTION('ref_axis',(0.,0.,1.));
#32777=DIRECTION('',(-1.,0.,0.));
#32778=DIRECTION('center_axis',(0.,1.,0.));
#32779=DIRECTION('ref_axis',(0.,0.,1.));
#32780=DIRECTION('',(-1.,0.,0.));
#32781=DIRECTION('center_axis',(0.,1.23292219708887E-16,1.));
#32782=DIRECTION('ref_axis',(0.,-1.,1.23292219708887E-16));
#32783=DIRECTION('center_axis',(0.,1.23292219708887E-16,-1.));
#32784=DIRECTION('ref_axis',(0.,1.,1.23292219708887E-16));
#40334=CARTESIAN_POINT('',(0.,0.,0.));
#40335=CARTESIAN_POINT('Origin',(1.,-9.3,2.45));
#40336=CARTESIAN_POINT('',(1.,-9.3,1.6));
#40337=CARTESIAN_POINT('Origin',(1.,-9.3,2.45));
#40338=CARTESIAN_POINT('',(0.,-9.3,1.6));
#40339=CARTESIAN_POINT('',(1.,-9.3,1.6));
#40340=CARTESIAN_POINT('Origin',(0.,-9.3,2.45));
#40341=CARTESIAN_POINT('Origin',(1.,-9.3,-2.45));
#40342=CARTESIAN_POINT('',(1.,-9.3,-3.3));
#40343=CARTESIAN_POINT('Origin',(1.,-9.3,-2.45));
#40344=CARTESIAN_POINT('',(0.,-9.3,-3.3));
#40345=CARTESIAN_POINT('',(1.,-9.3,-3.3));
#40346=CARTESIAN_POINT('Origin',(0.,-9.3,-2.45));
#40347=CARTESIAN_POINT('Origin',(1.,-0.55,0.));
#40348=CARTESIAN_POINT('',(1.,-7.68249605678125,0.499999999999999));
#40349=CARTESIAN_POINT('',(1.,-7.68249605678125,-0.5));
#40350=CARTESIAN_POINT('Origin',(1.,-0.55,0.));
#40351=CARTESIAN_POINT('',(0.,-7.68249605678125,0.499999999999999));
#40352=CARTESIAN_POINT('',(1.,-7.68249605678125,0.499999999999999));
#40353=CARTESIAN_POINT('',(0.,-7.68249605678125,-0.5));
#40354=CARTESIAN_POINT('Origin',(0.,-0.55,0.));
#40355=CARTESIAN_POINT('',(1.,-7.68249605678125,-0.5));
#40356=CARTESIAN_POINT('Origin',(1.,2.60208521396521E-15,2.71050543121376E-16));
#40357=CARTESIAN_POINT('',(1.,-7.14272206303279,-5.14018691588785));
#40358=CARTESIAN_POINT('',(1.,-7.14272206303279,5.14018691588785));
#40359=CARTESIAN_POINT('Origin',(1.,2.60208521396521E-15,2.71050543121376E-16));
#40360=CARTESIAN_POINT('',(0.,-7.14272206303279,-5.14018691588785));
#40361=CARTESIAN_POINT('',(1.,-7.14272206303279,-5.14018691588785));
#40362=CARTESIAN_POINT('',(0.,-7.14272206303279,5.14018691588785));
#40363=CARTESIAN_POINT('Origin',(0.,2.60208521396521E-15,2.71050543121376E-16));
#40364=CARTESIAN_POINT('',(1.,-7.14272206303279,5.14018691588785));
#40365=CARTESIAN_POINT('Origin',(1.,-0.55,0.));
#40366=CARTESIAN_POINT('',(1.,-11.2,-0.500000000000001));
#40367=CARTESIAN_POINT('',(1.,-11.2,-2.45));
#40368=CARTESIAN_POINT('',(1.,-11.2,-2.45));
#40369=CARTESIAN_POINT('',(1.,-9.3,-4.35));
#40370=CARTESIAN_POINT('Origin',(1.,-9.3,-2.45));
#40371=CARTESIAN_POINT('',(1.,-8.6849006902785,-4.35));
#40372=CARTESIAN_POINT('',(1.,-8.6849006902785,-4.35));
#40373=CARTESIAN_POINT('Origin',(1.,-8.6849006902785,-6.25));
#40374=CARTESIAN_POINT('',(1.,-8.6849006902785,4.35));
#40375=CARTESIAN_POINT('Origin',(1.,-8.6849006902785,6.25));
#40376=CARTESIAN_POINT('',(1.,-9.3,4.35));
#40377=CARTESIAN_POINT('',(1.,-8.6849006902785,4.35));
#40378=CARTESIAN_POINT('',(1.,-11.2,2.45));
#40379=CARTESIAN_POINT('Origin',(1.,-9.3,2.45));
#40380=CARTESIAN_POINT('',(1.,-11.2,0.500000000000001));
#40381=CARTESIAN_POINT('',(1.,-11.2,2.45));
#40382=CARTESIAN_POINT('',(1.,-7.68249605678125,0.5));
#40383=CARTESIAN_POINT('',(1.,-7.68249605678125,-0.5));
#40384=CARTESIAN_POINT('Origin',(0.,-0.55,0.));
#40385=CARTESIAN_POINT('',(0.,-11.2,-0.500000000000001));
#40386=CARTESIAN_POINT('',(0.,-11.2,-2.45));
#40387=CARTESIAN_POINT('',(0.,-11.2,-2.45));
#40388=CARTESIAN_POINT('',(0.,-7.68249605678125,-0.5));
#40389=CARTESIAN_POINT('',(0.,-11.2,0.500000000000001));
#40390=CARTESIAN_POINT('',(0.,-7.68249605678125,0.5));
#40391=CARTESIAN_POINT('',(0.,-11.2,2.45));
#40392=CARTESIAN_POINT('',(0.,-11.2,2.45));
#40393=CARTESIAN_POINT('',(0.,-9.3,4.35));
#40394=CARTESIAN_POINT('Origin',(0.,-9.3,2.45));
#40395=CARTESIAN_POINT('',(0.,-8.6849006902785,4.35));
#40396=CARTESIAN_POINT('',(0.,-8.6849006902785,4.35));
#40397=CARTESIAN_POINT('Origin',(0.,-8.6849006902785,6.25));
#40398=CARTESIAN_POINT('',(0.,-8.6849006902785,-4.35));
#40399=CARTESIAN_POINT('Origin',(0.,-8.6849006902785,-6.25));
#40400=CARTESIAN_POINT('',(0.,-9.3,-4.35));
#40401=CARTESIAN_POINT('',(0.,-8.6849006902785,-4.35));
#40402=CARTESIAN_POINT('Origin',(0.,-9.3,-2.45));
#40403=CARTESIAN_POINT('Origin',(1.,-11.2,-2.45));
#40404=CARTESIAN_POINT('',(1.,-11.2,-2.45));
#40405=CARTESIAN_POINT('',(1.,-11.2,-0.500000000000001));
#40406=CARTESIAN_POINT('Origin',(1.,-9.3,-2.45));
#40407=CARTESIAN_POINT('',(1.,-9.3,-4.35));
#40408=CARTESIAN_POINT('Origin',(1.,-8.6849006902785,-4.35));
#40409=CARTESIAN_POINT('',(1.,-8.6849006902785,-4.35));
#40410=CARTESIAN_POINT('Origin',(1.,-8.6849006902785,-6.25));
#40411=CARTESIAN_POINT('Origin',(1.,-8.6849006902785,6.25));
#40412=CARTESIAN_POINT('',(1.,-8.6849006902785,4.35));
#40413=CARTESIAN_POINT('Origin',(1.,-8.6849006902785,4.35));
#40414=CARTESIAN_POINT('',(1.,-9.3,4.35));
#40415=CARTESIAN_POINT('Origin',(1.,-9.3,2.45));
#40416=CARTESIAN_POINT('',(1.,-11.2,2.45));
#40417=CARTESIAN_POINT('Origin',(1.,-11.2,2.45));
#40418=CARTESIAN_POINT('',(1.,-11.2,0.500000000000001));
#40419=CARTESIAN_POINT('Origin',(1.,-7.68249605678125,0.5));
#40420=CARTESIAN_POINT('Origin',(1.,-7.68249605678125,-0.5));
#66658=UNCERTAINTY_MEASURE_WITH_UNIT(LENGTH_MEASURE(0.01),#66722,
'DISTANCE_ACCURACY_VALUE',
'Maximum model space distance between geometric entities at asserted c
onnectivities');
#66680=UNCERTAINTY_MEASURE_WITH_UNIT(LENGTH_MEASURE(0.01),#66722,
'DISTANCE_ACCURACY_VALUE',
'Maximum model space distance between geometric entities at asserted c
onnectivities');
#66699=(
GEOMETRIC_REPRESENTATION_CONTEXT(3)
GLOBAL_UNCERTAINTY_ASSIGNED_CONTEXT((#66658))
GLOBAL_UNIT_ASSIGNED_CONTEXT((#66722,#66724,#66725))
REPRESENTATION_CONTEXT('','3D')
);
#66721=(
GEOMETRIC_REPRESENTATION_CONTEXT(3)
GLOBAL_UNCERTAINTY_ASSIGNED_CONTEXT((#66680))
GLOBAL_UNIT_ASSIGNED_CONTEXT((#66722,#66724,#66725))
REPRESENTATION_CONTEXT('','3D')
);
#66722=(
LENGTH_UNIT()
NAMED_UNIT(*)
SI_UNIT(.MILLI.,.METRE.)
);
#66724=(
NAMED_UNIT(*)
PLANE_ANGLE_UNIT()
SI_UNIT($,.RADIAN.)
);
#66725=(
NAMED_UNIT(*)
SI_UNIT($,.STERADIAN.)
SOLID_ANGLE_UNIT()
);
#66744=SHAPE_DEFINITION_REPRESENTATION(#66798,#66908);
#66798=PRODUCT_DEFINITION_SHAPE('',$,#66949);
#66908=SHAPE_REPRESENTATION('',(#27435),#66699);
#66930=PRODUCT_DEFINITION_CONTEXT('part definition',#67052,'design');
#66949=PRODUCT_DEFINITION('Washer','Washer',#66989,#66930);
#66989=PRODUCT_DEFINITION_FORMATION('',$,#67072);
#67052=APPLICATION_CONTEXT(
'Core Data for Automotive Mechanical Design Process');
#67053=PRODUCT_CONTEXT('part definition',#67052,'mechanical');
#67072=PRODUCT('Washer','Washer',$,(#67053));
#67095=PRESENTATION_STYLE_ASSIGNMENT((#67097));
#67097=SURFACE_STYLE_USAGE(.BOTH.,#67099);
#67099=SURFACE_SIDE_STYLE('',(#67101));
#67101=SURFACE_STYLE_FILL_AREA(#67103);
#67103=FILL_AREA_STYLE('Opaque(202,209,238)',(#67105));
#67105=FILL_AREA_STYLE_COLOUR('Opaque(202,209,238)',#67107);
#67107=COLOUR_RGB('Opaque(202,209,238)',0.792156862745098,0.819607843137255,
0.933333333333333);
ENDSEC;
END-ISO-10303-21;
